ISO-10303-21;
HEADER;
/* Generated by software containing ST-Developer
 * from STEP Tools, Inc. (www.steptools.com) 
 */

FILE_DESCRIPTION(
/* description */ ('Gravity roller conveyor section'),
/* implementation_level */ '2;1');

FILE_NAME(
/* name */ 'Captive slot nut.step',
/* time_stamp */ '2026-11-02T07:43:02-08:00',
/* author */ (''),
/* organization */ (''),
/* preprocessor_version */ 'ST-DEVELOPER v20.2',
/* originating_system */ 'Autodesk Translation Framework v15.17.0.0',
/* authorisation */ '');

FILE_SCHEMA (('AUTOMOTIVE_DESIGN { 1 0 10303 214 3 1 1 }'));
ENDSEC;

DATA;
#10=MECHANICAL_DESIGN_GEOMETRIC_PRESENTATION_REPRESENTATION('',(#568),#13821);
#11=ELLIPSE('',#8670,0.299389011154384,0.2117);
#12=ELLIPSE('',#8674,0.299389011154384,0.2117);
#492=SHAPE_REPRESENTATION_RELATIONSHIP('SRR','None',#14031,#526);
#526=ADVANCED_BREP_SHAPE_REPRESENTATION('',(#607),#13818);
#568=STYLED_ITEM('',(#14192),#607);
#607=MANIFOLD_SOLID_BREP('Body1',#7669);
#692=FACE_BOUND('',#1888,.T.);
#975=PLANE('',#8660);
#976=PLANE('',#8661);
#977=PLANE('',#8662);
#978=PLANE('',#8664);
#979=PLANE('',#8665);
#980=PLANE('',#8666);
#981=PLANE('',#8667);
#982=PLANE('',#8668);
#983=PLANE('',#8669);
#984=PLANE('',#8676);
#985=PLANE('',#8677);
#986=PLANE('',#8678);
#987=PLANE('',#8679);
#1383=FACE_OUTER_BOUND('',#1885,.T.);
#1384=FACE_OUTER_BOUND('',#1886,.T.);
#1385=FACE_OUTER_BOUND('',#1887,.T.);
#1386=FACE_OUTER_BOUND('',#1889,.T.);
#1387=FACE_OUTER_BOUND('',#1890,.T.);
#1388=FACE_OUTER_BOUND('',#1891,.T.);
#1389=FACE_OUTER_BOUND('',#1892,.T.);
#1390=FACE_OUTER_BOUND('',#1893,.T.);
#1391=FACE_OUTER_BOUND('',#1894,.T.);
#1392=FACE_OUTER_BOUND('',#1895,.T.);
#1393=FACE_OUTER_BOUND('',#1896,.T.);
#1394=FACE_OUTER_BOUND('',#1897,.T.);
#1395=FACE_OUTER_BOUND('',#1898,.T.);
#1396=FACE_OUTER_BOUND('',#1899,.T.);
#1885=EDGE_LOOP('',(#6938,#6939,#6940,#6941));
#1886=EDGE_LOOP('',(#6942,#6943,#6944,#6945));
#1887=EDGE_LOOP('',(#6946,#6947,#6948,#6949));
#1888=EDGE_LOOP('',(#6950));
#1889=EDGE_LOOP('',(#6951,#6952,#6953,#6954,#6955,#6956,#6957,#6958,#6959,
#6960));
#1890=EDGE_LOOP('',(#6961,#6962,#6963,#6964));
#1891=EDGE_LOOP('',(#6965,#6966,#6967,#6968));
#1892=EDGE_LOOP('',(#6969,#6970,#6971,#6972,#6973,#6974,#6975,#6976,#6977,
#6978));
#1893=EDGE_LOOP('',(#6979,#6980,#6981,#6982));
#1894=EDGE_LOOP('',(#6983,#6984,#6985,#6986,#6987,#6988));
#1895=EDGE_LOOP('',(#6989,#6990,#6991,#6992,#6993,#6994,#6995,#6996));
#1896=EDGE_LOOP('',(#6997,#6998,#6999,#7000,#7001));
#1897=EDGE_LOOP('',(#7002,#7003,#7004,#7005));
#1898=EDGE_LOOP('',(#7006,#7007,#7008,#7009,#7010,#7011));
#1899=EDGE_LOOP('',(#7012,#7013,#7014,#7015));
#2583=LINE('',#13454,#3301);
#2584=LINE('',#13456,#3302);
#2585=LINE('',#13458,#3303);
#2586=LINE('',#13459,#3304);
#2587=LINE('',#13462,#3305);
#2588=LINE('',#13464,#3306);
#2589=LINE('',#13465,#3307);
#2590=LINE('',#13468,#3308);
#2591=LINE('',#13470,#3309);
#2592=LINE('',#13471,#3310);
#2593=LINE('',#13476,#3311);
#2594=LINE('',#13478,#3312);
#2595=LINE('',#13480,#3313);
#2596=LINE('',#13482,#3314);
#2597=LINE('',#13484,#3315);
#2598=LINE('',#13486,#3316);
#2599=LINE('',#13487,#3317);
#2600=LINE('',#13490,#3318);
#2601=LINE('',#13491,#3319);
#2602=LINE('',#13494,#3320);
#2603=LINE('',#13495,#3321);
#2604=LINE('',#13498,#3322);
#2605=LINE('',#13500,#3323);
#2606=LINE('',#13502,#3324);
#2607=LINE('',#13504,#3325);
#2608=LINE('',#13505,#3326);
#2609=LINE('',#13507,#3327);
#2610=LINE('',#13510,#3328);
#2611=LINE('',#13513,#3329);
#2612=LINE('',#13517,#3330);
#2613=LINE('',#13524,#3331);
#2614=LINE('',#13526,#3332);
#2615=LINE('',#13528,#3333);
#3301=VECTOR('',#10688,1.);
#3302=VECTOR('',#10689,1.);
#3303=VECTOR('',#10690,1.);
#3304=VECTOR('',#10691,1.);
#3305=VECTOR('',#10694,1.);
#3306=VECTOR('',#10695,1.);
#3307=VECTOR('',#10696,1.);
#3308=VECTOR('',#10699,1.);
#3309=VECTOR('',#10700,1.);
#3310=VECTOR('',#10701,1.);
#3311=VECTOR('',#10706,1.);
#3312=VECTOR('',#10707,1.);
#3313=VECTOR('',#10708,1.);
#3314=VECTOR('',#10709,1.);
#3315=VECTOR('',#10710,1.);
#3316=VECTOR('',#10711,1.);
#3317=VECTOR('',#10712,1.);
#3318=VECTOR('',#10715,1.);
#3319=VECTOR('',#10716,1.);
#3320=VECTOR('',#10719,1.);
#3321=VECTOR('',#10720,1.);
#3322=VECTOR('',#10723,1.);
#3323=VECTOR('',#10724,1.);
#3324=VECTOR('',#10725,1.);
#3325=VECTOR('',#10726,1.);
#3326=VECTOR('',#10727,1.);
#3327=VECTOR('',#10730,1.);
#3328=VECTOR('',#10733,1.);
#3329=VECTOR('',#10736,1.);
#3330=VECTOR('',#10741,0.21);
#3331=VECTOR('',#10750,1.);
#3332=VECTOR('',#10753,1.);
#3333=VECTOR('',#10756,1.);
#3569=CIRCLE('',#8663,0.2117);
#3570=CIRCLE('',#8672,0.2117);
#3571=CIRCLE('',#8673,0.2117);
#3572=CIRCLE('',#8675,0.2117);
#4175=VERTEX_POINT('',#13452);
#4176=VERTEX_POINT('',#13453);
#4177=VERTEX_POINT('',#13455);
#4178=VERTEX_POINT('',#13457);
#4179=VERTEX_POINT('',#13461);
#4180=VERTEX_POINT('',#13463);
#4181=VERTEX_POINT('',#13467);
#4182=VERTEX_POINT('',#13469);
#4183=VERTEX_POINT('',#13472);
#4184=VERTEX_POINT('',#13475);
#4185=VERTEX_POINT('',#13477);
#4186=VERTEX_POINT('',#13479);
#4187=VERTEX_POINT('',#13481);
#4188=VERTEX_POINT('',#13483);
#4189=VERTEX_POINT('',#13485);
#4190=VERTEX_POINT('',#13489);
#4191=VERTEX_POINT('',#13493);
#4192=VERTEX_POINT('',#13497);
#4193=VERTEX_POINT('',#13499);
#4194=VERTEX_POINT('',#13501);
#4195=VERTEX_POINT('',#13503);
#4196=VERTEX_POINT('',#13509);
#4197=VERTEX_POINT('',#13511);
#4198=VERTEX_POINT('',#13515);
#4199=VERTEX_POINT('',#13518);
#4200=VERTEX_POINT('',#13520);
#5106=EDGE_CURVE('',#4175,#4176,#2583,.T.);
#5107=EDGE_CURVE('',#4177,#4175,#2584,.T.);
#5108=EDGE_CURVE('',#4178,#4177,#2585,.T.);
#5109=EDGE_CURVE('',#4176,#4178,#2586,.T.);
#5110=EDGE_CURVE('',#4177,#4179,#2587,.T.);
#5111=EDGE_CURVE('',#4180,#4179,#2588,.T.);
#5112=EDGE_CURVE('',#4178,#4180,#2589,.T.);
#5113=EDGE_CURVE('',#4179,#4181,#2590,.T.);
#5114=EDGE_CURVE('',#4181,#4182,#2591,.T.);
#5115=EDGE_CURVE('',#4182,#4180,#2592,.T.);
#5116=EDGE_CURVE('',#4183,#4183,#3569,.T.);
#5117=EDGE_CURVE('',#4184,#4175,#2593,.T.);
#5118=EDGE_CURVE('',#4185,#4184,#2594,.T.);
#5119=EDGE_CURVE('',#4185,#4186,#2595,.T.);
#5120=EDGE_CURVE('',#4187,#4186,#2596,.T.);
#5121=EDGE_CURVE('',#4187,#4188,#2597,.T.);
#5122=EDGE_CURVE('',#4188,#4189,#2598,.T.);
#5123=EDGE_CURVE('',#4189,#4181,#2599,.T.);
#5124=EDGE_CURVE('',#4189,#4190,#2600,.T.);
#5125=EDGE_CURVE('',#4190,#4182,#2601,.T.);
#5126=EDGE_CURVE('',#4191,#4188,#2602,.T.);
#5127=EDGE_CURVE('',#4190,#4191,#2603,.T.);
#5128=EDGE_CURVE('',#4192,#4191,#2604,.T.);
#5129=EDGE_CURVE('',#4193,#4192,#2605,.T.);
#5130=EDGE_CURVE('',#4193,#4194,#2606,.T.);
#5131=EDGE_CURVE('',#4195,#4194,#2607,.T.);
#5132=EDGE_CURVE('',#4195,#4176,#2608,.T.);
#5133=EDGE_CURVE('',#4192,#4187,#2609,.T.);
#5134=EDGE_CURVE('',#4186,#4196,#2610,.T.);
#5135=EDGE_CURVE('',#4196,#4197,#11,.T.);
#5136=EDGE_CURVE('',#4197,#4193,#2611,.T.);
#5137=EDGE_CURVE('',#4198,#4196,#3570,.F.);
#5138=EDGE_CURVE('',#4198,#4183,#2612,.T.);
#5139=EDGE_CURVE('',#4199,#4198,#3571,.F.);
#5140=EDGE_CURVE('',#4200,#4199,#12,.T.);
#5141=EDGE_CURVE('',#4197,#4200,#3572,.F.);
#5142=EDGE_CURVE('',#4199,#4185,#2613,.T.);
#5143=EDGE_CURVE('',#4194,#4200,#2614,.T.);
#5144=EDGE_CURVE('',#4184,#4195,#2615,.T.);
#6938=ORIENTED_EDGE('',*,*,#5106,.F.);
#6939=ORIENTED_EDGE('',*,*,#5107,.F.);
#6940=ORIENTED_EDGE('',*,*,#5108,.F.);
#6941=ORIENTED_EDGE('',*,*,#5109,.F.);
#6942=ORIENTED_EDGE('',*,*,#5108,.T.);
#6943=ORIENTED_EDGE('',*,*,#5110,.T.);
#6944=ORIENTED_EDGE('',*,*,#5111,.F.);
#6945=ORIENTED_EDGE('',*,*,#5112,.F.);
#6946=ORIENTED_EDGE('',*,*,#5113,.T.);
#6947=ORIENTED_EDGE('',*,*,#5114,.T.);
#6948=ORIENTED_EDGE('',*,*,#5115,.T.);
#6949=ORIENTED_EDGE('',*,*,#5111,.T.);
#6950=ORIENTED_EDGE('',*,*,#5116,.T.);
#6951=ORIENTED_EDGE('',*,*,#5113,.F.);
#6952=ORIENTED_EDGE('',*,*,#5110,.F.);
#6953=ORIENTED_EDGE('',*,*,#5107,.T.);
#6954=ORIENTED_EDGE('',*,*,#5117,.F.);
#6955=ORIENTED_EDGE('',*,*,#5118,.F.);
#6956=ORIENTED_EDGE('',*,*,#5119,.T.);
#6957=ORIENTED_EDGE('',*,*,#5120,.F.);
#6958=ORIENTED_EDGE('',*,*,#5121,.T.);
#6959=ORIENTED_EDGE('',*,*,#5122,.T.);
#6960=ORIENTED_EDGE('',*,*,#5123,.T.);
#6961=ORIENTED_EDGE('',*,*,#5124,.T.);
#6962=ORIENTED_EDGE('',*,*,#5125,.T.);
#6963=ORIENTED_EDGE('',*,*,#5114,.F.);
#6964=ORIENTED_EDGE('',*,*,#5123,.F.);
#6965=ORIENTED_EDGE('',*,*,#5126,.F.);
#6966=ORIENTED_EDGE('',*,*,#5127,.F.);
#6967=ORIENTED_EDGE('',*,*,#5124,.F.);
#6968=ORIENTED_EDGE('',*,*,#5122,.F.);
#6969=ORIENTED_EDGE('',*,*,#5115,.F.);
#6970=ORIENTED_EDGE('',*,*,#5125,.F.);
#6971=ORIENTED_EDGE('',*,*,#5127,.T.);
#6972=ORIENTED_EDGE('',*,*,#5128,.F.);
#6973=ORIENTED_EDGE('',*,*,#5129,.F.);
#6974=ORIENTED_EDGE('',*,*,#5130,.T.);
#6975=ORIENTED_EDGE('',*,*,#5131,.F.);
#6976=ORIENTED_EDGE('',*,*,#5132,.T.);
#6977=ORIENTED_EDGE('',*,*,#5109,.T.);
#6978=ORIENTED_EDGE('',*,*,#5112,.T.);
#6979=ORIENTED_EDGE('',*,*,#5126,.T.);
#6980=ORIENTED_EDGE('',*,*,#5121,.F.);
#6981=ORIENTED_EDGE('',*,*,#5133,.F.);
#6982=ORIENTED_EDGE('',*,*,#5128,.T.);
#6983=ORIENTED_EDGE('',*,*,#5129,.T.);
#6984=ORIENTED_EDGE('',*,*,#5133,.T.);
#6985=ORIENTED_EDGE('',*,*,#5120,.T.);
#6986=ORIENTED_EDGE('',*,*,#5134,.T.);
#6987=ORIENTED_EDGE('',*,*,#5135,.T.);
#6988=ORIENTED_EDGE('',*,*,#5136,.T.);
#6989=ORIENTED_EDGE('',*,*,#5135,.F.);
#6990=ORIENTED_EDGE('',*,*,#5137,.F.);
#6991=ORIENTED_EDGE('',*,*,#5138,.T.);
#6992=ORIENTED_EDGE('',*,*,#5116,.F.);
#6993=ORIENTED_EDGE('',*,*,#5138,.F.);
#6994=ORIENTED_EDGE('',*,*,#5139,.F.);
#6995=ORIENTED_EDGE('',*,*,#5140,.F.);
#6996=ORIENTED_EDGE('',*,*,#5141,.F.);
#6997=ORIENTED_EDGE('',*,*,#5134,.F.);
#6998=ORIENTED_EDGE('',*,*,#5119,.F.);
#6999=ORIENTED_EDGE('',*,*,#5142,.F.);
#7000=ORIENTED_EDGE('',*,*,#5139,.T.);
#7001=ORIENTED_EDGE('',*,*,#5137,.T.);
#7002=ORIENTED_EDGE('',*,*,#5136,.F.);
#7003=ORIENTED_EDGE('',*,*,#5141,.T.);
#7004=ORIENTED_EDGE('',*,*,#5143,.F.);
#7005=ORIENTED_EDGE('',*,*,#5130,.F.);
#7006=ORIENTED_EDGE('',*,*,#5118,.T.);
#7007=ORIENTED_EDGE('',*,*,#5144,.T.);
#7008=ORIENTED_EDGE('',*,*,#5131,.T.);
#7009=ORIENTED_EDGE('',*,*,#5143,.T.);
#7010=ORIENTED_EDGE('',*,*,#5140,.T.);
#7011=ORIENTED_EDGE('',*,*,#5142,.T.);
#7012=ORIENTED_EDGE('',*,*,#5106,.T.);
#7013=ORIENTED_EDGE('',*,*,#5132,.F.);
#7014=ORIENTED_EDGE('',*,*,#5144,.F.);
#7015=ORIENTED_EDGE('',*,*,#5117,.T.);
#7200=CYLINDRICAL_SURFACE('',#8671,0.2117);
#7584=ADVANCED_FACE('',(#1383),#975,.F.);
#7585=ADVANCED_FACE('',(#1384),#976,.T.);
#7586=ADVANCED_FACE('',(#1385,#692),#977,.T.);
#7587=ADVANCED_FACE('',(#1386),#978,.T.);
#7588=ADVANCED_FACE('',(#1387),#979,.T.);
#7589=ADVANCED_FACE('',(#1388),#980,.F.);
#7590=ADVANCED_FACE('',(#1389),#981,.T.);
#7591=ADVANCED_FACE('',(#1390),#982,.T.);
#7592=ADVANCED_FACE('',(#1391),#983,.T.);
#7593=ADVANCED_FACE('',(#1392),#7200,.F.);
#7594=ADVANCED_FACE('',(#1393),#984,.F.);
#7595=ADVANCED_FACE('',(#1394),#985,.F.);
#7596=ADVANCED_FACE('',(#1395),#986,.T.);
#7597=ADVANCED_FACE('',(#1396),#987,.T.);
#7669=CLOSED_SHELL('',(#7584,#7585,#7586,#7587,#7588,#7589,#7590,#7591,
#7592,#7593,#7594,#7595,#7596,#7597));
#8659=AXIS2_PLACEMENT_3D('',#13450,#10684,#10685);
#8660=AXIS2_PLACEMENT_3D('',#13451,#10686,#10687);
#8661=AXIS2_PLACEMENT_3D('',#13460,#10692,#10693);
#8662=AXIS2_PLACEMENT_3D('',#13466,#10697,#10698);
#8663=AXIS2_PLACEMENT_3D('',#13473,#10702,#10703);
#8664=AXIS2_PLACEMENT_3D('',#13474,#10704,#10705);
#8665=AXIS2_PLACEMENT_3D('',#13488,#10713,#10714);
#8666=AXIS2_PLACEMENT_3D('',#13492,#10717,#10718);
#8667=AXIS2_PLACEMENT_3D('',#13496,#10721,#10722);
#8668=AXIS2_PLACEMENT_3D('',#13506,#10728,#10729);
#8669=AXIS2_PLACEMENT_3D('',#13508,#10731,#10732);
#8670=AXIS2_PLACEMENT_3D('',#13512,#10734,#10735);
#8671=AXIS2_PLACEMENT_3D('',#13514,#10737,#10738);
#8672=AXIS2_PLACEMENT_3D('',#13516,#10739,#10740);
#8673=AXIS2_PLACEMENT_3D('',#13519,#10742,#10743);
#8674=AXIS2_PLACEMENT_3D('',#13521,#10744,#10745);
#8675=AXIS2_PLACEMENT_3D('',#13522,#10746,#10747);
#8676=AXIS2_PLACEMENT_3D('',#13523,#10748,#10749);
#8677=AXIS2_PLACEMENT_3D('',#13525,#10751,#10752);
#8678=AXIS2_PLACEMENT_3D('',#13527,#10754,#10755);
#8679=AXIS2_PLACEMENT_3D('',#13529,#10757,#10758);
#10684=DIRECTION('axis',(0.,0.,1.));
#10685=DIRECTION('refdir',(1.,0.,0.));
#10686=DIRECTION('center_axis',(0.,0.,1.));
#10687=DIRECTION('ref_axis',(1.,0.,0.));
#10688=DIRECTION('',(1.,0.,0.));
#10689=DIRECTION('',(0.,-1.,0.));
#10690=DIRECTION('',(-1.,0.,0.));
#10691=DIRECTION('',(0.,1.,0.));
#10692=DIRECTION('center_axis',(0.,1.,0.));
#10693=DIRECTION('ref_axis',(-1.,0.,0.));
#10694=DIRECTION('',(0.,0.,1.));
#10695=DIRECTION('',(-1.,0.,0.));
#10696=DIRECTION('',(0.,0.,1.));
#10697=DIRECTION('center_axis',(0.,0.,1.));
#10698=DIRECTION('ref_axis',(1.,0.,0.));
#10699=DIRECTION('',(0.,-1.,0.));
#10700=DIRECTION('',(1.,0.,0.));
#10701=DIRECTION('',(0.,1.,0.));
#10702=DIRECTION('center_axis',(0.,0.,-1.));
#10703=DIRECTION('ref_axis',(1.,0.,0.));
#10704=DIRECTION('center_axis',(-1.,0.,0.));
#10705=DIRECTION('ref_axis',(0.,-1.,0.));
#10706=DIRECTION('',(0.,0.,1.));
#10707=DIRECTION('',(0.,0.707106781186548,0.707106781186548));
#10708=DIRECTION('',(0.,-1.,0.));
#10709=DIRECTION('',(0.,0.707106781186548,-0.707106781186548));
#10710=DIRECTION('',(0.,0.,1.));
#10711=DIRECTION('',(0.,-1.,0.));
#10712=DIRECTION('',(0.,0.,1.));
#10713=DIRECTION('center_axis',(0.,-1.,0.));
#10714=DIRECTION('ref_axis',(1.,0.,0.));
#10715=DIRECTION('',(1.,0.,0.));
#10716=DIRECTION('',(0.,0.,1.));
#10717=DIRECTION('center_axis',(0.,0.,1.));
#10718=DIRECTION('ref_axis',(1.,0.,0.));
#10719=DIRECTION('',(-1.,0.,0.));
#10720=DIRECTION('',(0.,1.,0.));
#10721=DIRECTION('center_axis',(1.,0.,0.));
#10722=DIRECTION('ref_axis',(0.,1.,0.));
#10723=DIRECTION('',(0.,0.,1.));
#10724=DIRECTION('',(0.,-0.707106781186548,0.707106781186548));
#10725=DIRECTION('',(0.,1.,0.));
#10726=DIRECTION('',(0.,-0.707106781186548,-0.707106781186548));
#10727=DIRECTION('',(0.,0.,1.));
#10728=DIRECTION('center_axis',(0.,-1.,0.));
#10729=DIRECTION('ref_axis',(1.,0.,0.));
#10730=DIRECTION('',(-1.,0.,0.));
#10731=DIRECTION('center_axis',(0.,-0.707106781186548,-0.707106781186548));
#10732=DIRECTION('ref_axis',(-1.,0.,0.));
#10733=DIRECTION('',(1.,0.,0.));
#10734=DIRECTION('center_axis',(0.,0.707106781186548,0.707106781186548));
#10735=DIRECTION('ref_axis',(0.,0.707106781186547,-0.707106781186547));
#10736=DIRECTION('',(1.,0.,0.));
#10737=DIRECTION('center_axis',(0.,0.,1.));
#10738=DIRECTION('ref_axis',(1.,0.,0.));
#10739=DIRECTION('center_axis',(0.,0.,-1.));
#10740=DIRECTION('ref_axis',(1.,0.,0.));
#10741=DIRECTION('',(0.,0.,1.));
#10742=DIRECTION('center_axis',(0.,0.,-1.));
#10743=DIRECTION('ref_axis',(1.,0.,0.));
#10744=DIRECTION('center_axis',(0.,-0.707106781186548,0.707106781186548));
#10745=DIRECTION('ref_axis',(0.,0.707106781186547,0.707106781186547));
#10746=DIRECTION('center_axis',(0.,0.,-1.));
#10747=DIRECTION('ref_axis',(1.,0.,0.));
#10748=DIRECTION('center_axis',(0.,0.,1.));
#10749=DIRECTION('ref_axis',(1.,0.,0.));
#10750=DIRECTION('',(-1.,0.,0.));
#10751=DIRECTION('center_axis',(0.,0.,1.));
#10752=DIRECTION('ref_axis',(1.,0.,0.));
#10753=DIRECTION('',(-1.,0.,0.));
#10754=DIRECTION('center_axis',(0.,0.707106781186548,-0.707106781186548));
#10755=DIRECTION('ref_axis',(-1.,0.,0.));
#10756=DIRECTION('',(1.,0.,0.));
#10757=DIRECTION('center_axis',(0.,1.,0.));
#10758=DIRECTION('ref_axis',(-1.,0.,0.));
#13450=CARTESIAN_POINT('',(0.,0.,0.));
#13451=CARTESIAN_POINT('Origin',(0.,0.395,0.25));
#13452=CARTESIAN_POINT('',(-0.5,0.3,0.25));
#13453=CARTESIAN_POINT('',(0.5,0.3,0.25));
#13454=CARTESIAN_POINT('',(0.25,0.3,0.25));
#13455=CARTESIAN_POINT('',(-0.5,0.5,0.25));
#13456=CARTESIAN_POINT('',(-0.5,0.5,0.25));
#13457=CARTESIAN_POINT('',(0.5,0.5,0.25));
#13458=CARTESIAN_POINT('',(0.5,0.5,0.25));
#13459=CARTESIAN_POINT('',(0.5,0.29,0.25));
#13460=CARTESIAN_POINT('Origin',(0.5,0.5,0.25));
#13461=CARTESIAN_POINT('',(-0.5,0.5,0.4));
#13462=CARTESIAN_POINT('',(-0.5,0.5,0.25));
#13463=CARTESIAN_POINT('',(0.5,0.5,0.4));
#13464=CARTESIAN_POINT('',(0.5,0.5,0.4));
#13465=CARTESIAN_POINT('',(0.5,0.5,0.25));
#13466=CARTESIAN_POINT('Origin',(0.,0.,0.4));
#13467=CARTESIAN_POINT('',(-0.5,-0.5,0.4));
#13468=CARTESIAN_POINT('',(-0.5,0.5,0.4));
#13469=CARTESIAN_POINT('',(0.5,-0.5,0.4));
#13470=CARTESIAN_POINT('',(-0.5,-0.5,0.4));
#13471=CARTESIAN_POINT('',(0.5,-0.3,0.4));
#13472=CARTESIAN_POINT('',(-0.2117,2.59257727379495E-17,0.4));
#13473=CARTESIAN_POINT('Origin',(0.,0.,0.4));
#13474=CARTESIAN_POINT('Origin',(-0.5,0.3,0.));
#13475=CARTESIAN_POINT('',(-0.5,0.3,0.15));
#13476=CARTESIAN_POINT('',(-0.5,0.3,0.));
#13477=CARTESIAN_POINT('',(-0.5,0.15,0.));
#13478=CARTESIAN_POINT('',(-0.5,0.225,0.075));
#13479=CARTESIAN_POINT('',(-0.5,-0.15,0.));
#13480=CARTESIAN_POINT('',(-0.5,0.3,0.));
#13481=CARTESIAN_POINT('',(-0.5,-0.3,0.15));
#13482=CARTESIAN_POINT('',(-0.5,-0.075,-0.075));
#13483=CARTESIAN_POINT('',(-0.5,-0.3,0.25));
#13484=CARTESIAN_POINT('',(-0.5,-0.3,0.));
#13485=CARTESIAN_POINT('',(-0.5,-0.5,0.25));
#13486=CARTESIAN_POINT('',(-0.5,-0.29,0.25));
#13487=CARTESIAN_POINT('',(-0.5,-0.5,0.25));
#13488=CARTESIAN_POINT('Origin',(-0.5,-0.5,0.25));
#13489=CARTESIAN_POINT('',(0.5,-0.5,0.25));
#13490=CARTESIAN_POINT('',(-0.5,-0.5,0.25));
#13491=CARTESIAN_POINT('',(0.5,-0.5,0.25));
#13492=CARTESIAN_POINT('Origin',(0.,-0.395,0.25));
#13493=CARTESIAN_POINT('',(0.5,-0.3,0.25));
#13494=CARTESIAN_POINT('',(-0.25,-0.3,0.25));
#13495=CARTESIAN_POINT('',(0.5,-0.5,0.25));
#13496=CARTESIAN_POINT('Origin',(0.5,-0.3,0.));
#13497=CARTESIAN_POINT('',(0.5,-0.3,0.15));
#13498=CARTESIAN_POINT('',(0.5,-0.3,0.));
#13499=CARTESIAN_POINT('',(0.5,-0.15,0.));
#13500=CARTESIAN_POINT('',(0.5,-0.225,0.075));
#13501=CARTESIAN_POINT('',(0.5,0.15,0.));
#13502=CARTESIAN_POINT('',(0.5,-0.3,0.));
#13503=CARTESIAN_POINT('',(0.5,0.3,0.15));
#13504=CARTESIAN_POINT('',(0.5,0.075,-0.075));
#13505=CARTESIAN_POINT('',(0.5,0.3,0.));
#13506=CARTESIAN_POINT('Origin',(-0.5,-0.3,0.));
#13507=CARTESIAN_POINT('',(-0.25,-0.3,0.15));
#13508=CARTESIAN_POINT('Origin',(-0.25,-0.225,0.075));
#13509=CARTESIAN_POINT('',(-0.149388386429468,-0.15,0.));
#13510=CARTESIAN_POINT('',(-0.25,-0.15,0.));
#13511=CARTESIAN_POINT('',(0.149388386429468,-0.15,0.));
#13512=CARTESIAN_POINT('Origin',(0.,0.,-0.15));
#13513=CARTESIAN_POINT('',(-0.25,-0.15,0.));
#13514=CARTESIAN_POINT('Origin',(0.,0.,-0.1));
#13515=CARTESIAN_POINT('',(-0.2117,-2.59257727379495E-17,0.));
#13516=CARTESIAN_POINT('Origin',(0.,0.,0.));
#13517=CARTESIAN_POINT('',(-0.2117,-2.59257727379495E-17,-0.1));
#13518=CARTESIAN_POINT('',(-0.149388386429468,0.15,0.));
#13519=CARTESIAN_POINT('Origin',(0.,0.,0.));
#13520=CARTESIAN_POINT('',(0.149388386429468,0.15,0.));
#13521=CARTESIAN_POINT('Origin',(0.,0.,-0.15));
#13522=CARTESIAN_POINT('Origin',(0.,0.,0.));
#13523=CARTESIAN_POINT('Origin',(0.,0.,0.));
#13524=CARTESIAN_POINT('',(0.25,0.15,0.));
#13525=CARTESIAN_POINT('Origin',(0.,0.,0.));
#13526=CARTESIAN_POINT('',(0.25,0.15,0.));
#13527=CARTESIAN_POINT('Origin',(0.25,0.225,0.075));
#13528=CARTESIAN_POINT('',(0.25,0.3,0.15));
#13529=CARTESIAN_POINT('Origin',(0.5,0.3,0.));
#13779=UNCERTAINTY_MEASURE_WITH_UNIT(LENGTH_MEASURE(0.001),#13822,
'DISTANCE_ACCURACY_VALUE',
'Maximum model space distance between geometric entities at asserted c
onnectivities');
#13782=UNCERTAINTY_MEASURE_WITH_UNIT(LENGTH_MEASURE(0.001),#13822,
'DISTANCE_ACCURACY_VALUE',
'Maximum model space distance between geometric entities at asserted c
onnectivities');
#13818=(
GEOMETRIC_REPRESENTATION_CONTEXT(3)
GLOBAL_UNCERTAINTY_ASSIGNED_CONTEXT((#13779))
GLOBAL_UNIT_ASSIGNED_CONTEXT((#13822,#13824,#13825))
REPRESENTATION_CONTEXT('','3D')
);
#13821=(
GEOMETRIC_REPRESENTATION_CONTEXT(3)
GLOBAL_UNCERTAINTY_ASSIGNED_CONTEXT((#13782))
GLOBAL_UNIT_ASSIGNED_CONTEXT((#13822,#13824,#13825))
REPRESENTATION_CONTEXT('','3D')
);
#13822=(
LENGTH_UNIT()
NAMED_UNIT(*)
SI_UNIT(.CENTI.,.METRE.)
);
#13824=(
NAMED_UNIT(*)
PLANE_ANGLE_UNIT()
SI_UNIT($,.RADIAN.)
);
#13825=(
NAMED_UNIT(*)
SI_UNIT($,.STERADIAN.)
SOLID_ANGLE_UNIT()
);
#13861=SHAPE_DEFINITION_REPRESENTATION(#13904,#14031);
#13904=PRODUCT_DEFINITION_SHAPE('',$,#14070);
#14031=SHAPE_REPRESENTATION('',(#8659),#13818);
#14034=PRODUCT_DEFINITION_CONTEXT('part definition',#14150,'design');
#14070=PRODUCT_DEFINITION('Captive slot nut','Captive slot nut',#14108,
#14034);
#14108=PRODUCT_DEFINITION_FORMATION('',$,#14187);
#14150=APPLICATION_CONTEXT(
'Core Data for Automotive Mechanical Design Process');
#14151=PRODUCT_CONTEXT('part definition',#14150,'mechanical');
#14187=PRODUCT('Captive slot nut','Captive slot nut','Captive slot nut',
(#14151));
#14192=PRESENTATION_STYLE_ASSIGNMENT((#14197));
#14197=SURFACE_STYLE_USAGE(.BOTH.,#14202);
#14202=SURFACE_SIDE_STYLE('',(#14207));
#14207=SURFACE_STYLE_FILL_AREA(#14212);
#14212=FILL_AREA_STYLE('CAD Library Painted - Engineering blue',(#14217));
#14217=FILL_AREA_STYLE_COLOUR('CAD Library Painted - Engineering blue',
#14222);
#14222=COLOUR_RGB('CAD Library Painted - Engineering blue',0.12156862745098,
0.356862745098039,0.6);
ENDSEC;
END-ISO-10303-21;
